ISO-10303-21;
HEADER;
/* Generated by software containing ST-Developer
 * from STEP Tools, Inc. (www.steptools.com) 
 */

FILE_DESCRIPTION(
/* description */ (''),
/* implementation_level */ '2;1');

FILE_NAME(
/* name */ 'Pin_03.step',
/* time_stamp */ '2026-10-23T17:00:58+06:00',
/* author */ (''),
/* organization */ (''),
/* preprocessor_version */ 'ST-DEVELOPER v20.2',
/* originating_system */ 'Autodesk Translation Framework v15.15.0.0',
/* authorisation */ '');

FILE_SCHEMA (('AUTOMOTIVE_DESIGN { 1 0 10303 214 3 1 1 }'));
ENDSEC;

DATA;
#10=MECHANICAL_DESIGN_GEOMETRIC_PRESENTATION_REPRESENTATION('',(#115),#11385);
#89=SHAPE_REPRESENTATION_RELATIONSHIP('SRR','None',#11441,#102);
#102=ADVANCED_BREP_SHAPE_REPRESENTATION('',(#128),#11381);
#115=STYLED_ITEM('',(#11567),#128);
#128=MANIFOLD_SOLID_BREP('Pin_03',#5351);
#268=CONICAL_SURFACE('',#6050,0.7,0.785398163397451);
#269=CONICAL_SURFACE('',#6056,0.7,0.785398163397448);
#516=CIRCLE('',#6051,0.649999999999999);
#517=CIRCLE('',#6052,0.75);
#518=CIRCLE('',#6054,0.75);
#519=CIRCLE('',#6057,0.649999999999999);
#601=CYLINDRICAL_SURFACE('',#6053,0.75);
#904=FACE_OUTER_BOUND('',#1268,.T.);
#905=FACE_OUTER_BOUND('',#1269,.T.);
#906=FACE_OUTER_BOUND('',#1270,.T.);
#907=FACE_OUTER_BOUND('',#1271,.T.);
#908=FACE_OUTER_BOUND('',#1272,.T.);
#1268=EDGE_LOOP('',(#4772,#4773,#4774,#4775));
#1269=EDGE_LOOP('',(#4776,#4777,#4778,#4779));
#1270=EDGE_LOOP('',(#4780));
#1271=EDGE_LOOP('',(#4781,#4782,#4783,#4784));
#1272=EDGE_LOOP('',(#4785));
#1733=LINE('',#10793,#2195);
#1734=LINE('',#10797,#2196);
#1735=LINE('',#10802,#2197);
#2195=VECTOR('',#7652,0.7);
#2196=VECTOR('',#7657,0.75);
#2197=VECTOR('',#7664,0.7);
#2634=VERTEX_POINT('',#10790);
#2635=VERTEX_POINT('',#10792);
#2636=VERTEX_POINT('',#10796);
#2637=VERTEX_POINT('',#10801);
#3351=EDGE_CURVE('',#2634,#2634,#516,.T.);
#3352=EDGE_CURVE('',#2634,#2635,#1733,.T.);
#3353=EDGE_CURVE('',#2635,#2635,#517,.T.);
#3354=EDGE_CURVE('',#2635,#2636,#1734,.T.);
#3355=EDGE_CURVE('',#2636,#2636,#518,.T.);
#3356=EDGE_CURVE('',#2636,#2637,#1735,.T.);
#3357=EDGE_CURVE('',#2637,#2637,#519,.T.);
#4772=ORIENTED_EDGE('',*,*,#3351,.F.);
#4773=ORIENTED_EDGE('',*,*,#3352,.T.);
#4774=ORIENTED_EDGE('',*,*,#3353,.F.);
#4775=ORIENTED_EDGE('',*,*,#3352,.F.);
#4776=ORIENTED_EDGE('',*,*,#3353,.T.);
#4777=ORIENTED_EDGE('',*,*,#3354,.T.);
#4778=ORIENTED_EDGE('',*,*,#3355,.T.);
#4779=ORIENTED_EDGE('',*,*,#3354,.F.);
#4780=ORIENTED_EDGE('',*,*,#3351,.T.);
#4781=ORIENTED_EDGE('',*,*,#3355,.F.);
#4782=ORIENTED_EDGE('',*,*,#3356,.T.);
#4783=ORIENTED_EDGE('',*,*,#3357,.F.);
#4784=ORIENTED_EDGE('',*,*,#3356,.F.);
#4785=ORIENTED_EDGE('',*,*,#3357,.T.);
#5002=PLANE('',#6055);
#5003=PLANE('',#6058);
#5316=ADVANCED_FACE('',(#904),#268,.T.);
#5317=ADVANCED_FACE('',(#905),#601,.T.);
#5318=ADVANCED_FACE('',(#906),#5002,.F.);
#5319=ADVANCED_FACE('',(#907),#269,.T.);
#5320=ADVANCED_FACE('',(#908),#5003,.T.);
#5351=CLOSED_SHELL('',(#5316,#5317,#5318,#5319,#5320));
#6049=AXIS2_PLACEMENT_3D('',#10788,#7646,#7647);
#6050=AXIS2_PLACEMENT_3D('',#10789,#7648,#7649);
#6051=AXIS2_PLACEMENT_3D('',#10791,#7650,#7651);
#6052=AXIS2_PLACEMENT_3D('',#10794,#7653,#7654);
#6053=AXIS2_PLACEMENT_3D('',#10795,#7655,#7656);
#6054=AXIS2_PLACEMENT_3D('',#10798,#7658,#7659);
#6055=AXIS2_PLACEMENT_3D('',#10799,#7660,#7661);
#6056=AXIS2_PLACEMENT_3D('',#10800,#7662,#7663);
#6057=AXIS2_PLACEMENT_3D('',#10803,#7665,#7666);
#6058=AXIS2_PLACEMENT_3D('',#10804,#7667,#7668);
#7646=DIRECTION('axis',(0.,0.,1.));
#7647=DIRECTION('refdir',(1.,0.,0.));
#7648=DIRECTION('center_axis',(2.22044604925031E-16,-1.,-1.22464679914735E-16));
#7649=DIRECTION('ref_axis',(-1.,-2.22044604925031E-16,-2.71926214689378E-32));
#7650=DIRECTION('center_axis',(-2.22044604925031E-16,1.,1.22464679914735E-16));
#7651=DIRECTION('ref_axis',(-1.,-2.22044604925031E-16,-2.71926214689378E-32));
#7652=DIRECTION('',(0.70710678118655,-0.707106781186545,4.95239128556718E-31));
#7653=DIRECTION('center_axis',(2.22044604925031E-16,-1.,-1.22464679914735E-16));
#7654=DIRECTION('ref_axis',(-1.,-2.22044604925031E-16,-2.71926214689378E-32));
#7655=DIRECTION('center_axis',(2.22044604925031E-16,-1.,-1.22464679914735E-16));
#7656=DIRECTION('ref_axis',(-1.,-2.22044604925031E-16,-2.71926214689378E-32));
#7657=DIRECTION('',(2.22044604925031E-16,-1.,-1.22464679914735E-16));
#7658=DIRECTION('center_axis',(-2.22044604925031E-16,1.,1.22464679914735E-16));
#7659=DIRECTION('ref_axis',(-1.,-2.22044604925031E-16,-2.71926214689378E-32));
#7660=DIRECTION('center_axis',(2.22044604925031E-16,-1.,-1.22464679914735E-16));
#7661=DIRECTION('ref_axis',(0.,-1.22464679914735E-16,1.));
#7662=DIRECTION('center_axis',(-2.22044604925031E-16,1.,1.22464679914735E-16));
#7663=DIRECTION('ref_axis',(-1.,-2.22044604925031E-16,-2.71926214689378E-32));
#7664=DIRECTION('',(-0.707106781186547,-0.707106781186548,-1.73191211247099E-16));
#7665=DIRECTION('center_axis',(2.22044604925031E-16,-1.,-1.22464679914735E-16));
#7666=DIRECTION('ref_axis',(-1.,-2.22044604925031E-16,-2.71926214689378E-32));
#7667=DIRECTION('center_axis',(2.22044604925031E-16,-1.,-1.22464679914735E-16));
#7668=DIRECTION('ref_axis',(0.,-1.22464679914735E-16,1.));
#10788=CARTESIAN_POINT('',(0.,0.,0.));
#10789=CARTESIAN_POINT('Origin',(-18.7359120418715,27.7504782148047,17.6));
#10790=CARTESIAN_POINT('',(-18.0859120418715,27.8004782148047,17.6));
#10791=CARTESIAN_POINT('Origin',(-18.7359120418715,27.8004782148047,17.6));
#10792=CARTESIAN_POINT('',(-17.9859120418715,27.7004782148047,17.6));
#10793=CARTESIAN_POINT('',(-18.0359120418715,27.7504782148047,17.6));
#10794=CARTESIAN_POINT('Origin',(-18.7359120418715,27.7004782148047,17.6));
#10795=CARTESIAN_POINT('Origin',(-18.7359120418715,22.4004782148047,17.6));
#10796=CARTESIAN_POINT('',(-17.9859120418715,22.5004782148047,17.6));
#10797=CARTESIAN_POINT('',(-17.9859120418715,22.4004782148047,17.6));
#10798=CARTESIAN_POINT('Origin',(-18.7359120418715,22.5004782148047,17.6));
#10799=CARTESIAN_POINT('Origin',(-18.7359120418715,27.8004782148047,17.6));
#10800=CARTESIAN_POINT('Origin',(-18.7359120418715,22.4504782148047,17.6));
#10801=CARTESIAN_POINT('',(-18.0859120418715,22.4004782148047,17.6));
#10802=CARTESIAN_POINT('',(-18.0359120418715,22.4504782148047,17.6));
#10803=CARTESIAN_POINT('Origin',(-18.7359120418715,22.4004782148047,17.6));
#10804=CARTESIAN_POINT('Origin',(-18.7359120418715,22.4004782148047,17.6));
#11366=UNCERTAINTY_MEASURE_WITH_UNIT(LENGTH_MEASURE(0.01),#11386,
'DISTANCE_ACCURACY_VALUE',
'Maximum model space distance between geometric entities at asserted c
onnectivities');
#11370=UNCERTAINTY_MEASURE_WITH_UNIT(LENGTH_MEASURE(0.01),#11386,
'DISTANCE_ACCURACY_VALUE',
'Maximum model space distance between geometric entities at asserted c
onnectivities');
#11381=(
GEOMETRIC_REPRESENTATION_CONTEXT(3)
GLOBAL_UNCERTAINTY_ASSIGNED_CONTEXT((#11366))
GLOBAL_UNIT_ASSIGNED_CONTEXT((#11386,#11388,#11389))
REPRESENTATION_CONTEXT('','3D')
);
#11385=(
GEOMETRIC_REPRESENTATION_CONTEXT(3)
GLOBAL_UNCERTAINTY_ASSIGNED_CONTEXT((#11370))
GLOBAL_UNIT_ASSIGNED_CONTEXT((#11386,#11388,#11389))
REPRESENTATION_CONTEXT('','3D')
);
#11386=(
LENGTH_UNIT()
NAMED_UNIT(*)
SI_UNIT(.MILLI.,.METRE.)
);
#11388=(
NAMED_UNIT(*)
PLANE_ANGLE_UNIT()
SI_UNIT($,.RADIAN.)
);
#11389=(
NAMED_UNIT(*)
SI_UNIT($,.STERADIAN.)
SOLID_ANGLE_UNIT()
);
#11400=SHAPE_DEFINITION_REPRESENTATION(#11414,#11441);
#11414=PRODUCT_DEFINITION_SHAPE('',$,#11456);
#11441=SHAPE_REPRESENTATION('',(#6049),#11381);
#11445=PRODUCT_DEFINITION_CONTEXT('part definition',#11489,'design');
#11456=PRODUCT_DEFINITION('Pin_03','Pin_03',#11470,#11445);
#11470=PRODUCT_DEFINITION_FORMATION('',$,#11501);
#11489=APPLICATION_CONTEXT(
'Core Data for Automotive Mechanical Design Process');
#11490=PRODUCT_CONTEXT('part definition',#11489,'mechanical');
#11501=PRODUCT('Pin_03','Pin_03',$,(#11490));
#11561=COLOUR_RGB('Grey',0.48,0.52,0.57);
#11562=FILL_AREA_STYLE_COLOUR('',#11561);
#11563=FILL_AREA_STYLE('',(#11562));
#11564=SURFACE_STYLE_FILL_AREA(#11563);
#11565=SURFACE_SIDE_STYLE('',(#11564));
#11566=SURFACE_STYLE_USAGE(.BOTH.,#11565);
#11567=PRESENTATION_STYLE_ASSIGNMENT((#11566));
ENDSEC;
END-ISO-10303-21;
